ISO-10303-21;
HEADER;
/* Generated by software containing ST-Developer
 * from STEP Tools, Inc. (www.steptools.com) 
 */

FILE_DESCRIPTION(
/* description */ ('STEP AP214'),
/* implementation_level */ '2;1');

FILE_NAME(
/* name */ 'PUR-BR-9003.step',
/* time_stamp */ '2026-10-07T12:49:37-07:00',
/* author */ (''),
/* organization */ (''),
/* preprocessor_version */ 'ST-DEVELOPER v20.2',
/* originating_system */ 'Autodesk Translation Framework v15.15.0.0',
/* authorisation */ '');

FILE_SCHEMA (('AUTOMOTIVE_DESIGN { 1 0 10303 214 3 1 1 }'));
ENDSEC;

DATA;
#10=MECHANICAL_DESIGN_GEOMETRIC_PRESENTATION_REPRESENTATION('',(#294),#33016);
#177=SPHERICAL_SURFACE('',#10689,2.75);
#240=SHAPE_REPRESENTATION_RELATIONSHIP('SRR','None',#33133,#267);
#267=ADVANCED_BREP_SHAPE_REPRESENTATION('',(#325),#32994);
#294=STYLED_ITEM('',(#33286),#325);
#325=MANIFOLD_SOLID_BREP('Body1',#9949);
#1268=FACE_OUTER_BOUND('',#1846,.T.);
#1846=EDGE_LOOP('',(#7722,#7723));
#2395=CIRCLE('',#10690,2.75);
#4523=VERTEX_POINT('',#21076);
#4524=VERTEX_POINT('',#21077);
#5674=EDGE_CURVE('',#4523,#4524,#2395,.T.);
#7722=ORIENTED_EDGE('',*,*,#5674,.T.);
#7723=ORIENTED_EDGE('',*,*,#5674,.F.);
#9634=ADVANCED_FACE('',(#1268),#177,.T.);
#9949=CLOSED_SHELL('',(#9634));
#10688=AXIS2_PLACEMENT_3D('',#21074,#12489,#12490);
#10689=AXIS2_PLACEMENT_3D('',#21075,#12491,#12492);
#10690=AXIS2_PLACEMENT_3D('',#21078,#12493,#12494);
#12489=DIRECTION('axis',(0.,0.,1.));
#12490=DIRECTION('refdir',(1.,0.,0.));
#12491=DIRECTION('center_axis',(-1.,5.55111512312579E-17,6.12323399573673E-17));
#12492=DIRECTION('ref_axis',(-4.07638157631888E-31,2.09541177949331E-31,
1.));
#12493=DIRECTION('center_axis',(-5.55111512312579E-17,-1.,1.22464679914736E-16));
#12494=DIRECTION('ref_axis',(4.00840002264653E-31,-1.22464679914736E-16,
-1.));
#21074=CARTESIAN_POINT('',(0.,0.,0.));
#21075=CARTESIAN_POINT('Origin',(0.,0.,0.));
#21076=CARTESIAN_POINT('',(-2.75,1.52655665885959E-16,-1.68388934882762E-16));
#21077=CARTESIAN_POINT('',(2.75,-1.52655665885959E-16,-1.6838893488276E-16));
#21078=CARTESIAN_POINT('Origin',(0.,0.,0.));
#32962=UNCERTAINTY_MEASURE_WITH_UNIT(LENGTH_MEASURE(0.01),#33017,
'DISTANCE_ACCURACY_VALUE',
'Maximum model space distance between geometric entities at asserted c
onnectivities');
#32984=UNCERTAINTY_MEASURE_WITH_UNIT(LENGTH_MEASURE(0.01),#33017,
'DISTANCE_ACCURACY_VALUE',
'Maximum model space distance between geometric entities at asserted c
onnectivities');
#32994=(
GEOMETRIC_REPRESENTATION_CONTEXT(3)
GLOBAL_UNCERTAINTY_ASSIGNED_CONTEXT((#32962))
GLOBAL_UNIT_ASSIGNED_CONTEXT((#33017,#33019,#33020))
REPRESENTATION_CONTEXT('','3D')
);
#33016=(
GEOMETRIC_REPRESENTATION_CONTEXT(3)
GLOBAL_UNCERTAINTY_ASSIGNED_CONTEXT((#32984))
GLOBAL_UNIT_ASSIGNED_CONTEXT((#33017,#33019,#33020))
REPRESENTATION_CONTEXT('','3D')
);
#33017=(
LENGTH_UNIT()
NAMED_UNIT(*)
SI_UNIT(.MILLI.,.METRE.)
);
#33019=(
NAMED_UNIT(*)
PLANE_ANGLE_UNIT()
SI_UNIT($,.RADIAN.)
);
#33020=(
NAMED_UNIT(*)
SI_UNIT($,.STERADIAN.)
SOLID_ANGLE_UNIT()
);
#33030=SHAPE_DEFINITION_REPRESENTATION(#33061,#33133);
#33061=PRODUCT_DEFINITION_SHAPE('',$,#33165);
#33133=SHAPE_REPRESENTATION('',(#10688),#32994);
#33155=PRODUCT_DEFINITION_CONTEXT('part definition',#33250,'design');
#33165=PRODUCT_DEFINITION('BO21-001_Ball_PUR-BR-9003_M_Rev00',
'PUR-BR-9003',#33196,#33155);
#33196=PRODUCT_DEFINITION_FORMATION('',$,#33261);
#33250=APPLICATION_CONTEXT(
'Core Data for Automotive Mechanical Design Process');
#33251=PRODUCT_CONTEXT('part definition',#33250,'mechanical');
#33261=PRODUCT('BO21-001_Ball_PUR-BR-9003_M_Rev00','PUR-BR-9003',$,(#33251));
#33286=PRESENTATION_STYLE_ASSIGNMENT((#33293));
#33293=SURFACE_STYLE_USAGE(.BOTH.,#33300);
#33300=SURFACE_SIDE_STYLE('',(#33307));
#33307=SURFACE_STYLE_FILL_AREA(#33314);
#33314=FILL_AREA_STYLE('Opaque(178,178,178)',(#33321));
#33321=FILL_AREA_STYLE_COLOUR('Opaque(178,178,178)',#33328);
#33328=COLOUR_RGB('Opaque(178,178,178)', 0.66274510, 0.83137255, 0.94901961);
ENDSEC;
END-ISO-10303-21;
